ISO-10303-21;
HEADER;
FILE_DESCRIPTION (('STEP AP214'),
    '1' );
FILE_NAME ('slotted pan head screw_iso_ISO 1580 - M4 x 12 - 12N.step',
    '2026-10-27T08:02:39',
    ( '' ),
    ( '' ),
    'SwSTEP 2.0',
    'SolidWorks 2026',
    '' );
FILE_SCHEMA (( 'AUTOMOTIVE_DESIGN' ));
ENDSEC;

DATA;
#54=CIRCLE ( 'NONE', #10234, 3.873645755336797780 ) ;
#89=AXIS2_PLACEMENT_3D ( 'NONE', #7473, #7293, #11207 ) ;
#90=DIRECTION ( 'NONE',  ( -1.000000000000000000, -0.000000000000000000, -0.000000000000000000 ) ) ;
#158=ORIENTED_EDGE ( 'NONE', *, *, #10534, .F. ) ;
#169=CIRCLE ( 'NONE', #368, 3.873645755336797780 ) ;
#212=CARTESIAN_POINT ( 'NONE',  ( 0.000000000000000000, 0.000000000000000000, 0.000000000000000000 ) ) ;
#233=( NAMED_UNIT ( * ) SI_UNIT ( $, .STERADIAN. ) SOLID_ANGLE_UNIT ( ) );
#254=DIRECTION ( 'NONE',  ( 0.000000000000000000, 0.000000000000000000, 1.000000000000000000 ) ) ;
#261=CARTESIAN_POINT ( 'NONE',  ( 14.39999999999999680, 0.000000000000000000, 0.000000000000000000 ) ) ;
#280=MANIFOLD_SOLID_BREP ( 'Slot', #7978 ) ;
#309=DIRECTION ( 'NONE',  ( -1.000000000000000000, -0.000000000000000000, -0.000000000000000000 ) ) ;
#329=CARTESIAN_POINT ( 'NONE',  ( 1.000000000000000000, 4.743847875303940761E-16, -3.873645755336797780 ) ) ;
#340=ADVANCED_FACE ( 'NONE', ( #2436 ), #5125, .T. ) ;
#368=AXIS2_PLACEMENT_3D ( 'NONE', #1356, #11728, #9996 ) ;
#389=DIRECTION ( 'NONE',  ( 0.000000000000000000, 0.000000000000000000, -1.000000000000000000 ) ) ;
#391=CARTESIAN_POINT ( 'NONE',  ( 2.399999999999999467, 4.898587196589413815E-16, 4.000000000000000000 ) ) ;
#400=CARTESIAN_POINT ( 'NONE',  ( 0.09947414737648539729, 0.5999999999999997558, -3.189051013155320469 ) ) ;
#405=LINE ( 'NONE', #1345, #2435 ) ;
#418=AXIS2_PLACEMENT_3D ( 'NONE', #10477, #3731, #9491 ) ;
#452=FACE_BOUND ( 'NONE', #11698, .T. ) ;
#465=ORIENTED_EDGE ( 'NONE', *, *, #560, .F. ) ;
#496=CARTESIAN_POINT ( 'NONE',  ( 0.1893088852826965152, 0.6000000000000000888, 3.298489774147015829 ) ) ;
#505=CARTESIAN_POINT ( 'NONE',  ( 0.7248882449525384519, -0.5999999999999994227, -3.753866745206998701 ) ) ;
#544=DIRECTION ( 'NONE',  ( 0.000000000000000000, 0.000000000000000000, -1.000000000000000000 ) ) ;
#549=CARTESIAN_POINT ( 'NONE',  ( 0.3704956024625865041, 0.5999999999999998668, 3.518228334340779195 ) ) ;
#560=EDGE_CURVE ( 'NONE', #11027, #12039, #1005, .T. ) ;
#676=ADVANCED_FACE ( 'NONE', ( #1939 ), #5688, .T. ) ;
#766=DIRECTION ( 'NONE',  ( 0.000000000000000000, 0.000000000000000000, 1.000000000000000000 ) ) ;
#819=CARTESIAN_POINT ( 'NONE',  ( 1.095413108702814053, 4.828698707966718301E-16, 3.885863436426969297 ) ) ;
#913=CYLINDRICAL_SURFACE ( 'NONE', #418, 2.000000000000000000 ) ;
#950=CARTESIAN_POINT ( 'NONE',  ( 1.000000000000000000, -0.5999999999999994227, -4.000000000000000000 ) ) ;
#972=VERTEX_POINT ( 'NONE', #6546 ) ;
#990=FACE_OUTER_BOUND ( 'NONE', #7425, .T. ) ;
#995=CARTESIAN_POINT ( 'NONE',  ( 0.8601259673543576456, -0.6000000000000000888, 3.802963942891089300 ) ) ;
#1005=CIRCLE ( 'NONE', #9001, 4.000000000000000000 ) ;
#1061=EDGE_LOOP ( 'NONE', ( #11023, #10557 ) ) ;
#1072=LINE ( 'NONE', #9514, #12068 ) ;
#1121=ORIENTED_EDGE ( 'NONE', *, *, #4874, .F. ) ;
#1138=ADVANCED_FACE ( 'NONE', ( #6614 ), #3794, .F. ) ;
#1170=DIRECTION ( 'NONE',  ( -0.000000000000000000, 0.000000000000000000, 1.000000000000000000 ) ) ;
#1226=CARTESIAN_POINT ( 'NONE',  ( 1.000000000000000000, 0.5999999999999998668, -3.826895796574397046 ) ) ;
#1231=ORIENTED_EDGE ( 'NONE', *, *, #10376, .T. ) ;
#1238=CIRCLE ( 'NONE', #8627, 2.690429798716874377 ) ;
#1239=CARTESIAN_POINT ( 'NONE',  ( -25.39999999999996305, 0.000000000000000000, 2.000000000000000000 ) ) ;
#1258=DIRECTION ( 'NONE',  ( -1.000000000000000000, 0.000000000000000000, 0.000000000000000000 ) ) ;
#1273=EDGE_CURVE ( 'NONE', #6083, #7961, #3680, .T. ) ;
#1291=ORIENTED_EDGE ( 'NONE', *, *, #1273, .T. ) ;
#1294=EDGE_CURVE ( 'NONE', #5455, #1899, #2602, .T. ) ;
#1332=EDGE_CURVE ( 'NONE', #9795, #6083, #1421, .T. ) ;
#1344=ADVANCED_FACE ( 'NONE', ( #3533 ), #12207, .T. ) ;
#1345=CARTESIAN_POINT ( 'NONE',  ( 0.000000000000000000, 0.5999999999999998668, 4.000000000000000000 ) ) ;
#1356=CARTESIAN_POINT ( 'NONE',  ( 1.000000000000000000, 0.000000000000000000, 0.000000000000000000 ) ) ;
#1390=CARTESIAN_POINT ( 'NONE',  ( 1.000000000000000000, 0.5999999999999998668, 4.000000000000000000 ) ) ;
#1406=ORIENTED_EDGE ( 'NONE', *, *, #8447, .F. ) ;
#1421=CIRCLE ( 'NONE', #7422, 2.690429798716874377 ) ;
#1436=FACE_OUTER_BOUND ( 'NONE', #11778, .T. ) ;
#1451=CARTESIAN_POINT ( 'NONE',  ( 0.1191357322639439581, -0.5999999999999995337, -3.174145254273323058 ) ) ;
#1593=ORIENTED_EDGE ( 'NONE', *, *, #7120, .T. ) ;
#1614=CARTESIAN_POINT ( 'NONE',  ( 0.000000000000000000, 0.000000000000000000, 0.000000000000000000 ) ) ;
#1648=ORIENTED_EDGE ( 'NONE', *, *, #6328, .T. ) ;
#1771=( NAMED_UNIT ( * ) SI_UNIT ( $, .STERADIAN. ) SOLID_ANGLE_UNIT ( ) );
#1797=CIRCLE ( 'NONE', #10779, 4.000000000000000000 ) ;
#1847=VECTOR ( 'NONE', #309, 1000.000000000000000 ) ;
#1899=VERTEX_POINT ( 'NONE', #819 ) ;
#1939=FACE_OUTER_BOUND ( 'NONE', #1061, .T. ) ;
#1940=CARTESIAN_POINT ( 'NONE',  ( 0.4797447997155618316, -0.6000000000000003109, 3.611077595140663288 ) ) ;
#1947=EDGE_CURVE ( 'NONE', #9611, #7959, #4806, .T. ) ;
#1967=CARTESIAN_POINT ( 'NONE',  ( 2.399999999999999467, 0.000000000000000000, 0.000000000000000000 ) ) ;
#1993=STYLED_ITEM('',(#12405),#280);
#1995=ORIENTED_EDGE ( 'NONE', *, *, #7120, .F. ) ;
#2002=DIRECTION ( 'NONE',  ( 0.000000000000000000, 8.881784197001252323E-15, 1.000000000000000000 ) ) ;
#2010=FACE_OUTER_BOUND ( 'NONE', #6120, .T. ) ;
#2013=DIRECTION ( 'NONE',  ( -1.000000000000000000, -0.000000000000000000, -0.000000000000000000 ) ) ;
#2017=DIRECTION ( 'NONE',  ( -1.000000000000000000, -0.000000000000000000, -0.000000000000000000 ) ) ;
#2039=VECTOR ( 'NONE', #389, 1000.000000000000000 ) ;
#2042=ORIENTED_EDGE ( 'NONE', *, *, #11893, .F. ) ;
#2059=EDGE_LOOP ( 'NONE', ( #4091, #10923 ) ) ;
#2065=EDGE_CURVE ( 'NONE', #6664, #11679, #2601, .T. ) ;
#2071=EDGE_LOOP ( 'NONE', ( #2454, #7760, #5751, #1995 ) ) ;
#2123=ORIENTED_EDGE ( 'NONE', *, *, #8447, .T. ) ;
#2141=ORIENTED_EDGE ( 'NONE', *, *, #8087, .T. ) ;
#2222=DIRECTION ( 'NONE',  ( -1.000000000000000000, -0.000000000000000000, -0.000000000000000000 ) ) ;
#2223=CARTESIAN_POINT ( 'NONE',  ( 1.095413108702814053, 0.000000000000000000, 0.000000000000000000 ) ) ;
#2230=SURFACE_STYLE_USAGE ( .BOTH. , #3124 ) ;
#2261=CARTESIAN_POINT ( 'NONE',  ( 1.000000000000000000, -0.5999999999999995337, -3.826895796574397046 ) ) ;
#2326=LINE ( 'NONE', #1390, #2039 ) ;
#2358=LINE ( 'NONE', #10745, #1847 ) ;
#2435=VECTOR ( 'NONE', #8930, 1000.000000000000000 ) ;
#2436=FACE_OUTER_BOUND ( 'NONE', #12125, .T. ) ;
#2443=ORIENTED_EDGE ( 'NONE', *, *, #2933, .F. ) ;
#2444=CARTESIAN_POINT ( 'NONE',  ( 0.3700949531097381118, -0.5999999999999994227, -3.517837443070535919 ) ) ;
#2454=ORIENTED_EDGE ( 'NONE', *, *, #2065, .T. ) ;
#2601=CIRCLE ( 'NONE', #11585, 2.000000000000000000 ) ;
#2602=CIRCLE ( 'NONE', #6209, 3.885863436426969297 ) ;
#2612=AXIS2_PLACEMENT_3D ( 'NONE', #4728, #12282, #10341 ) ;
#2631=( GEOMETRIC_REPRESENTATION_CONTEXT ( 3 ) GLOBAL_UNCERTAINTY_ASSIGNED_CONTEXT ( ( #10519 ) ) GLOBAL_UNIT_ASSIGNED_CONTEXT ( ( #10862, #4054, #233 ) ) REPRESENTATION_CONTEXT ( 'NONE', 'WORKASPACE' ) );
#2717=EDGE_CURVE ( 'NONE', #4999, #6297, #1238, .T. ) ;
#2725=FACE_OUTER_BOUND ( 'NONE', #2071, .T. ) ;
#2726=CARTESIAN_POINT ( 'NONE',  ( 1.199999999999999956, 0.000000000000000000, 0.000000000000000000 ) ) ;
#2750=PLANE ( 'NONE',  #7583 ) ;
#2784=FACE_OUTER_BOUND ( 'NONE', #5487, .T. ) ;
#2801=DIRECTION ( 'NONE',  ( 0.000000000000000000, 0.000000000000000000, -1.000000000000000000 ) ) ;
#2854=PRODUCT_CONTEXT ( 'NONE', #4738, 'mechanical' ) ;
#2865=CARTESIAN_POINT ( 'NONE',  ( 0.4795650472149387000, 0.5999999999999996447, 3.611001245881807264 ) ) ;
#2898=LINE ( 'NONE', #2950, #7041 ) ;
#2933=EDGE_CURVE ( 'NONE', #1899, #5455, #9630, .T. ) ;
#2937=CARTESIAN_POINT ( 'NONE',  ( 1.000000000000000000, 0.000000000000000000, 0.000000000000000000 ) ) ;
#2943=DIRECTION ( 'NONE',  ( 0.000000000000000000, 9.486769009248163798E-17, -1.000000000000000000 ) ) ;
#2950=CARTESIAN_POINT ( 'NONE',  ( 0.000000000000000000, 0.000000000000000000, -3.790027207537782772 ) ) ;
#2977=CARTESIAN_POINT ( 'NONE',  ( 1.000000000000000000, 0.5999999999999998668, -3.826895796574397046 ) ) ;
#2978=CARTESIAN_POINT ( 'NONE',  ( 1.000000000000000000, 0.5999999999999998668, 4.000000000000000000 ) ) ;
#2989=DIRECTION ( 'NONE',  ( 0.000000000000000000, 0.000000000000000000, -1.000000000000000000 ) ) ;
#2990=VERTEX_POINT ( 'NONE', #329 ) ;
#3021=LINE ( 'NONE', #950, #10272 ) ;
#3023=EDGE_CURVE ( 'NONE', #972, #7961, #2326, .T. ) ;
#3088=CIRCLE ( 'NONE', #89, 3.873645755336797780 ) ;
#3124=SURFACE_SIDE_STYLE ('',( #11718 ) ) ;
#3127=ORIENTED_EDGE ( 'NONE', *, *, #12093, .T. ) ;
#3128=LINE ( 'NONE', #1239, #8357 ) ;
#3152=PRODUCT_DEFINITION_CONTEXT ( 'detailed design', #7311, 'design' ) ;
#3174=PRESENTATION_STYLE_ASSIGNMENT (( #2230 ) ) ;
#3180=DIRECTION ( 'NONE',  ( -1.000000000000000000, -0.000000000000000000, -0.000000000000000000 ) ) ;
#3184=ORIENTED_EDGE ( 'NONE', *, *, #4023, .F. ) ;
#3214=LINE ( 'NONE', #9955, #7837 ) ;
#3270=EDGE_CURVE ( 'NONE', #1899, #10913, #3641, .T. ) ;
#3336=EDGE_CURVE ( 'NONE', #5455, #12039, #2898, .T. ) ;
#3372=CARTESIAN_POINT ( 'NONE',  ( 1.000000000000000000, 0.5999999999999998668, 3.826895796574397046 ) ) ;
#3510=VERTEX_POINT ( 'NONE', #2261 ) ;
#3533=FACE_OUTER_BOUND ( 'NONE', #2059, .T. ) ;
#3595=DIRECTION ( 'NONE',  ( -1.000000000000000000, -0.000000000000000000, -0.000000000000000000 ) ) ;
#3622=AXIS2_PLACEMENT_3D ( 'NONE', #6989, #9877, #2989 ) ;
#3641=CIRCLE ( 'NONE', #7654, 1.199999999999999956 ) ;
#3680=B_SPLINE_CURVE_WITH_KNOTS ( 'NONE', 3,
 ( #9800, #11663, #400, #6108, #6926, #5154, #10727, #1226 ),
 .UNSPECIFIED., .F., .F.,
 ( 4, 2, 2, 4 ),
 ( 0.006406776852013720304, 0.007252600724735226365, 0.007675512661095979829, 0.008098424597456733293 ),
 .UNSPECIFIED. ) ;
#3731=DIRECTION ( 'NONE',  ( -1.000000000000000000, -0.000000000000000000, -0.000000000000000000 ) ) ;
#3753=DIRECTION ( 'NONE',  ( -0.000000000000000000, 1.000000000000000000, 1.224646799147353207E-16 ) ) ;
#3780=ORIENTED_EDGE ( 'NONE', *, *, #2717, .F. ) ;
#3794=PLANE ( 'NONE',  #11983 ) ;
#3804=( LENGTH_UNIT ( ) NAMED_UNIT ( * ) SI_UNIT ( .MILLI., .METRE. ) );
#3809=AXIS2_PLACEMENT_3D ( 'NONE', #5659, #5714, #6856 ) ;
#3810=EDGE_CURVE ( 'NONE', #3510, #2990, #54, .T. ) ;
#3831=CARTESIAN_POINT ( 'NONE',  ( 2.399999999999999467, 0.000000000000000000, 0.000000000000000000 ) ) ;
#3879=CARTESIAN_POINT ( 'NONE',  ( 0.000000000000000000, 0.000000000000000000, 0.000000000000000000 ) ) ;
#3932=DIRECTION ( 'NONE',  ( 0.000000000000000000, 0.000000000000000000, 1.000000000000000000 ) ) ;
#3944=ORIENTED_EDGE ( 'NONE', *, *, #1947, .T. ) ;
#3957=EDGE_LOOP ( 'NONE', ( #1291, #11999, #7681, #3127 ) ) ;
#4017=ORIENTED_EDGE ( 'NONE', *, *, #3336, .T. ) ;
#4023=EDGE_CURVE ( 'NONE', #3510, #4999, #4724, .T. ) ;
#4035=DIRECTION ( 'NONE',  ( 0.000000000000000000, 0.000000000000000000, 1.000000000000000000 ) ) ;
#4054=( NAMED_UNIT ( * ) PLANE_ANGLE_UNIT ( ) SI_UNIT ( $, .RADIAN. ) );
#4091=ORIENTED_EDGE ( 'NONE', *, *, #6328, .F. ) ;
#4151=CIRCLE ( 'NONE', #11761, 3.873645755336797780 ) ;
#4218=DIRECTION ( 'NONE',  ( 0.000000000000000000, 0.000000000000000000, 1.000000000000000000 ) ) ;
#4370=CARTESIAN_POINT ( 'NONE',  ( 0.8608560235772251268, -0.5999999999999993117, -3.803088852414125753 ) ) ;
#4450=ORIENTED_EDGE ( 'NONE', *, *, #3023, .T. ) ;
#4610=CARTESIAN_POINT ( 'NONE',  ( 0.8603041673727119809, 0.5999999999999998668, 3.802994432158365967 ) ) ;
#4619=PRODUCT_DEFINITION_SHAPE ( 'NONE', 'NONE',  #7780 ) ;
#4637=CARTESIAN_POINT ( 'NONE',  ( 14.39999999999999680, 2.449293598294706414E-16, -2.000000000000000000 ) ) ;
#4641=COLOUR_RGB ( '',1.000000000000000000, 0.9490196078431372140, 0.9098039215686274384 ) ;
#4658=EDGE_CURVE ( 'NONE', #2990, #7961, #3088, .T. ) ;
#4700=AXIS2_PLACEMENT_3D ( 'NONE', #1614, #11113, #544 ) ;
#4710=ORIENTED_EDGE ( 'NONE', *, *, #3810, .T. ) ;
#4724=B_SPLINE_CURVE_WITH_KNOTS ( 'NONE', 3,
 ( #10018, #4370, #505, #8322, #2444, #8200, #1451, #5451, #5381, #12113 ),
 .UNSPECIFIED., .F., .F.,
 ( 4, 2, 2, 2, 4 ),
 ( 0.007142761454519953000, 0.007565713830041730613, 0.007988666205563509093, 0.008411618581085286706, 0.008834570956607064318 ),
 .UNSPECIFIED. ) ;
#4727=ORIENTED_EDGE ( 'NONE', *, *, #2933, .T. ) ;
#4728=CARTESIAN_POINT ( 'NONE',  ( 1.199999999999999956, 0.000000000000000000, 0.000000000000000000 ) ) ;
#4738=APPLICATION_CONTEXT ( 'automotive_design' ) ;
#4748=ORIENTED_EDGE ( 'NONE', *, *, #4023, .T. ) ;
#4804=DIRECTION ( 'NONE',  ( 1.000000000000000000, 0.000000000000000000, 0.000000000000000000 ) ) ;
#4805=AXIS2_PLACEMENT_3D ( 'NONE', #1967, #90, #10660 ) ;
#4806=CIRCLE ( 'NONE', #8812, 2.000000000000000000 ) ;
#4810=CARTESIAN_POINT ( 'NONE',  ( 1.000000000000000000, -0.6000000000000001998, 3.826895796574397046 ) ) ;
#4833=MECHANICAL_DESIGN_GEOMETRIC_PRESENTATION_REPRESENTATION('',(#5039),#2631);
#4874=EDGE_CURVE ( 'NONE', #3510, #5352, #3021, .T. ) ;
#4886=ORIENTED_EDGE ( 'NONE', *, *, #11777, .T. ) ;
#4999=VERTEX_POINT ( 'NONE', #8909 ) ;
#5000=CARTESIAN_POINT ( 'NONE',  ( 14.39999999999999680, 0.000000000000000000, 2.000000000000000000 ) ) ;
#5038=ADVANCED_FACE ( 'NONE', ( #6958, #452 ), #10835, .F. ) ;
#5039=STYLED_ITEM ( 'NONE', ( #3174 ), #7504 ) ;
#5041=AXIS2_PLACEMENT_3D ( 'NONE', #7825, #3753, #6647 ) ;
#5052=ORIENTED_EDGE ( 'NONE', *, *, #8087, .F. ) ;
#5093=ORIENTED_EDGE ( 'NONE', *, *, #4658, .T. ) ;
#5125=PLANE ( 'NONE',  #9987 ) ;
#5134=ORIENTED_EDGE ( 'NONE', *, *, #3270, .T. ) ;
#5154=CARTESIAN_POINT ( 'NONE',  ( 0.7254551418982898570, 0.5999999999999999778, -3.754038125290899863 ) ) ;
#5199=DIRECTION ( 'NONE',  ( 0.000000000000000000, -9.486769009248163798E-17, 1.000000000000000000 ) ) ;
#5267=EDGE_CURVE ( 'NONE', #1899, #11027, #1072, .T. ) ;
#5316=CARTESIAN_POINT ( 'NONE',  ( 0.000000000000000000, 0.5999999999999998668, 2.622672778259560467 ) ) ;
#5352=VERTEX_POINT ( 'NONE', #6946 ) ;
#5381=CARTESIAN_POINT ( 'NONE',  ( -4.065758146820644093E-17, -0.5999999999999994227, -2.765548208259129837 ) ) ;
#5443=CIRCLE ( 'NONE', #10233, 2.000000000000000000 ) ;
#5451=CARTESIAN_POINT ( 'NONE',  ( 0.02377697851851289651, -0.5999999999999995337, -2.905229528491392266 ) ) ;
#5455=VERTEX_POINT ( 'NONE', #9762 ) ;
#5487=EDGE_LOOP ( 'NONE', ( #10598, #2443, #5134, #8940, #10100, #3780, #3184, #4710 ) ) ;
#5541=ADVANCED_FACE ( 'NONE', ( #1436 ), #9904, .T. ) ;
#5583=ORIENTED_EDGE ( 'NONE', *, *, #3270, .F. ) ;
#5594=CIRCLE ( 'NONE', #4805, 2.000000000000000000 ) ;
#5599=FACE_OUTER_BOUND ( 'NONE', #7433, .T. ) ;
#5636=CARTESIAN_POINT ( 'NONE',  ( 1.000000000000000000, -0.5999999999999994227, -4.000000000000000000 ) ) ;
#5659=CARTESIAN_POINT ( 'NONE',  ( -25.39999999999996305, 0.000000000000000000, 0.000000000000000000 ) ) ;
#5675=DIRECTION ( 'NONE',  ( 0.000000000000000000, 1.000000000000000000, 0.000000000000000000 ) ) ;
#5688=PLANE ( 'NONE',  #11175 ) ;
#5699=DIRECTION ( 'NONE',  ( 0.000000000000000000, -1.000000000000000000, -9.486769009248163798E-17 ) ) ;
#5706=CARTESIAN_POINT ( 'NONE',  ( 1.199999999999999956, 0.000000000000000000, 2.690429798716874377 ) ) ;
#5714=DIRECTION ( 'NONE',  ( -1.000000000000000000, -0.000000000000000000, -0.000000000000000000 ) ) ;
#5743=CARTESIAN_POINT ( 'NONE',  ( 0.09977878429777278790, -0.6000000000000000888, 3.189823563989766964 ) ) ;
#5751=ORIENTED_EDGE ( 'NONE', *, *, #1947, .F. ) ;
#5814=CARTESIAN_POINT ( 'NONE',  ( -3.444205370125434777E-14, -0.6000000000000000888, 2.905564161116319877 ) ) ;
#5867=ORIENTED_EDGE ( 'NONE', *, *, #4874, .T. ) ;
#5877=SHAPE_REPRESENTATION ( 'slotted pan head screw_iso_ISO 1580 - M4 x 12 - 12N', ( #6056 ), #10030 ) ;
#5888=CARTESIAN_POINT ( 'NONE',  ( 0.7245795732250854826, -0.6000000000000001998, 3.753610258581185910 ) ) ;
#5897=ADVANCED_FACE ( 'NONE', ( #11671 ), #11607, .T. ) ;
#5931=FILL_AREA_STYLE_COLOUR ( '', #4641 ) ;
#5974=AXIS2_PLACEMENT_3D ( 'NONE', #2726, #8606, #12283 ) ;
#6056=AXIS2_PLACEMENT_3D ( 'NONE', #212, #4035, #8864 ) ;
#6083=VERTEX_POINT ( 'NONE', #10058 ) ;
#6092=AXIS2_PLACEMENT_3D ( 'NONE', #7906, #9777, #8776 ) ;
#6093=ADVANCED_FACE ( 'NONE', ( #5599 ), #8021, .T. ) ;
#6108=CARTESIAN_POINT ( 'NONE',  ( 0.3688486069976970039, 0.6000000000000000888, -3.516473936516294252 ) ) ;
#6120=EDGE_LOOP ( 'NONE', ( #4748, #1648, #1231, #1121 ) ) ;
#6149=ADVANCED_FACE ( 'NONE', ( #2725 ), #913, .T. ) ;
#6209=AXIS2_PLACEMENT_3D ( 'NONE', #2223, #9871, #4218 ) ;
#6213=ORIENTED_EDGE ( 'NONE', *, *, #2065, .F. ) ;
#6297=VERTEX_POINT ( 'NONE', #11699 ) ;
#6328=EDGE_CURVE ( 'NONE', #4999, #6297, #3214, .T. ) ;
#6349=DIRECTION ( 'NONE',  ( 0.000000000000000000, 0.000000000000000000, 1.000000000000000000 ) ) ;
#6378=EDGE_LOOP ( 'NONE', ( #6213, #8741 ) ) ;
#6534=DIRECTION ( 'NONE',  ( -1.000000000000000000, -0.000000000000000000, -0.000000000000000000 ) ) ;
#6546=CARTESIAN_POINT ( 'NONE',  ( 1.000000000000000000, 0.5999999999999998668, 3.826895796574397046 ) ) ;
#6603=ADVANCED_FACE ( 'NONE', ( #2010 ), #2750, .F. ) ;
#6614=FACE_OUTER_BOUND ( 'NONE', #3957, .T. ) ;
#6623=ORIENTED_EDGE ( 'NONE', *, *, #1294, .F. ) ;
#6647=DIRECTION ( 'NONE',  ( 0.000000000000000000, -1.224646799147352961E-16, 1.000000000000000000 ) ) ;
#6661=EDGE_CURVE ( 'NONE', #10913, #5352, #4151, .T. ) ;
#6664=VERTEX_POINT ( 'NONE', #5000 ) ;
#6666=UNCERTAINTY_MEASURE_WITH_UNIT (LENGTH_MEASURE( 1.000000000000000082E-05 ), #3804, 'distance_accuracy_value', 'NONE');
#6673=CARTESIAN_POINT ( 'NONE',  ( 1.095413108702814053, 0.000000000000000000, 0.000000000000000000 ) ) ;
#6686=CARTESIAN_POINT ( 'NONE',  ( 2.399999999999999467, 2.449293598294706414E-16, -2.000000000000000000 ) ) ;
#6700=CARTESIAN_POINT ( 'NONE',  ( -7.839872433920653082E-18, 0.000000000000000000, 0.000000000000000000 ) ) ;
#6718=CARTESIAN_POINT ( 'NONE',  ( 14.39999999999999680, 0.000000000000000000, 0.000000000000000000 ) ) ;
#6719=DIRECTION ( 'NONE',  ( 0.9961946980917455452, 0.000000000000000000, -0.08715574274765813811 ) ) ;
#6725=DIRECTION ( 'NONE',  ( 0.000000000000000000, -9.486769009248163798E-17, 1.000000000000000000 ) ) ;
#6739=ORIENTED_EDGE ( 'NONE', *, *, #5267, .F. ) ;
#6754=CARTESIAN_POINT ( 'NONE',  ( 0.000000000000000000, -0.6000000000000000888, 2.622672778259560467 ) ) ;
#6755=DIRECTION ( 'NONE',  ( 1.000000000000000000, -0.000000000000000000, -0.000000000000000000 ) ) ;
#6767=DIRECTION ( 'NONE',  ( 0.000000000000000000, 0.000000000000000000, 1.000000000000000000 ) ) ;
#6802=DIRECTION ( 'NONE',  ( 0.000000000000000000, -0.000000000000000000, 1.000000000000000000 ) ) ;
#6810=SHAPE_REPRESENTATION_RELATIONSHIP ( 'NONE' , 'NONE' ,  #5877, #7504 ) ;
#6821=EDGE_LOOP ( 'NONE', ( #5052, #465 ) ) ;
#6843=DIRECTION ( 'NONE',  ( 0.000000000000000000, -1.000000000000000000, 0.000000000000000000 ) ) ;
#6856=DIRECTION ( 'NONE',  ( 0.000000000000000000, 0.000000000000000000, 1.000000000000000000 ) ) ;
#6901=DIRECTION ( 'NONE',  ( -1.000000000000000000, -0.000000000000000000, -0.000000000000000000 ) ) ;
#6926=CARTESIAN_POINT ( 'NONE',  ( 0.4798950312200447876, 0.5999999999999998668, -3.611246565534919739 ) ) ;
#6946=CARTESIAN_POINT ( 'NONE',  ( 1.000000000000000000, -0.6000000000000001998, 3.826895796574397046 ) ) ;
#6958=FACE_OUTER_BOUND ( 'NONE', #6821, .T. ) ;
#6989=CARTESIAN_POINT ( 'NONE',  ( 14.40000000000000036, 2.000000000000000000, 0.000000000000000000 ) ) ;
#7041=VECTOR ( 'NONE', #6719, 1000.000000000000000 ) ;
#7078=ADVANCED_FACE ( 'NONE', ( #990 ), #7564, .T. ) ;
#7120=EDGE_CURVE ( 'NONE', #6664, #9611, #3128, .T. ) ;
#7194=( GEOMETRIC_REPRESENTATION_CONTEXT ( 3 ) GLOBAL_UNCERTAINTY_ASSIGNED_CONTEXT ( ( #9542 ) ) GLOBAL_UNIT_ASSIGNED_CONTEXT ( ( #10397, #7670, #1771 ) ) REPRESENTATION_CONTEXT ( 'NONE', 'WORKASPACE' ) );
#7293=DIRECTION ( 'NONE',  ( 1.000000000000000000, -0.000000000000000000, -0.000000000000000000 ) ) ;
#7311=APPLICATION_CONTEXT ( 'automotive_design' ) ;
#7422=AXIS2_PLACEMENT_3D ( 'NONE', #8413, #3595, #766 ) ;
#7425=EDGE_LOOP ( 'NONE', ( #6739, #4727, #4017, #2141 ) ) ;
#7433=EDGE_LOOP ( 'NONE', ( #6623, #4886, #5093, #12061, #8130, #11286, #10017, #5583 ) ) ;
#7473=CARTESIAN_POINT ( 'NONE',  ( 1.000000000000000000, 0.000000000000000000, 0.000000000000000000 ) ) ;
#7475=ADVANCED_FACE ( 'NONE', ( #2784 ), #8977, .T. ) ;
#7480=DIRECTION ( 'NONE',  ( -0.000000000000000000, 0.000000000000000000, 1.000000000000000000 ) ) ;
#7504=ADVANCED_BREP_SHAPE_REPRESENTATION ( '', ( #280, #6056 ), #10030 ) ;
#7564=CONICAL_SURFACE ( 'NONE', #9563, 3.790027207537782772, 0.08726646259971644615 ) ;
#7583=AXIS2_PLACEMENT_3D ( 'NONE', #5636, #5699, #2943 ) ;
#7594=FACE_OUTER_BOUND ( 'NONE', #8001, .T. ) ;
#7630=AXIS2_PLACEMENT_3D ( 'NONE', #6673, #10470, #7860 ) ;
#7654=AXIS2_PLACEMENT_3D ( 'NONE', #5706, #6843, #8522 ) ;
#7670=( NAMED_UNIT ( * ) PLANE_ANGLE_UNIT ( ) SI_UNIT ( $, .RADIAN. ) );
#7681=ORIENTED_EDGE ( 'NONE', *, *, #8917, .T. ) ;
#7724=CYLINDRICAL_SURFACE ( 'NONE', #3809, 2.000000000000000000 ) ;
#7730=PRODUCT ( 'slotted pan head screw_iso_ISO 1580 - M4 x 12 - 12N', 'slotted pan head screw_iso_ISO 1580 - M4 x 12 - 12N', '', ( #2854 ) ) ;
#7760=ORIENTED_EDGE ( 'NONE', *, *, #11893, .T. ) ;
#7780=PRODUCT_DEFINITION ( 'UNKNOWN', '', #11226, #3152 ) ;
#7825=CARTESIAN_POINT ( 'NONE',  ( 1.199999999999999956, 3.294826241329278276E-16, -2.690429798716874377 ) ) ;
#7837=VECTOR ( 'NONE', #5199, 1000.000000000000000 ) ;
#7860=DIRECTION ( 'NONE',  ( 0.000000000000000000, 0.000000000000000000, 1.000000000000000000 ) ) ;
#7906=CARTESIAN_POINT ( 'NONE',  ( 2.399999999999999467, 2.000000000000000000, 0.000000000000000000 ) ) ;
#7959=VERTEX_POINT ( 'NONE', #6686 ) ;
#7961=VERTEX_POINT ( 'NONE', #2977 ) ;
#7978=CLOSED_SHELL ( 'NONE', ( #6093, #5541, #6149, #676, #8463, #5897, #1344, #7078, #5038, #7475, #1138, #6603, #340 ) ) ;
#8001=EDGE_LOOP ( 'NONE', ( #2042, #12275, #1593, #1406 ) ) ;
#8021=TOROIDAL_SURFACE ( 'NONE', #2612, 2.690429798716874377, 1.199999999999999956 ) ;
#8058=CARTESIAN_POINT ( 'NONE',  ( 2.399999999999999467, 0.000000000000000000, 0.000000000000000000 ) ) ;
#8063=CARTESIAN_POINT ( 'NONE',  ( 2.399999999999999467, 0.000000000000000000, -4.000000000000000000 ) ) ;
#8087=EDGE_CURVE ( 'NONE', #12039, #11027, #1797, .T. ) ;
#8115=DIRECTION ( 'NONE',  ( 0.000000000000000000, 0.000000000000000000, 1.000000000000000000 ) ) ;
#8130=ORIENTED_EDGE ( 'NONE', *, *, #1332, .F. ) ;
#8173=ORIENTED_EDGE ( 'NONE', *, *, #5267, .T. ) ;
#8193=CARTESIAN_POINT ( 'NONE',  ( 0.7251148409942000939, 0.5999999999999998668, 3.753893533104442071 ) ) ;
#8200=CARTESIAN_POINT ( 'NONE',  ( 0.1890552205643245831, -0.5999999999999995337, -3.298086786345711285 ) ) ;
#8322=CARTESIAN_POINT ( 'NONE',  ( 0.4784740205221562626, -0.5999999999999993117, -3.610260709030697956 ) ) ;
#8357=VECTOR ( 'NONE', #3180, 1000.000000000000000 ) ;
#8413=CARTESIAN_POINT ( 'NONE',  ( 0.000000000000000000, 0.000000000000000000, 0.000000000000000000 ) ) ;
#8446=CARTESIAN_POINT ( 'NONE',  ( 2.399999999999999467, 0.000000000000000000, 0.000000000000000000 ) ) ;
#8447=EDGE_CURVE ( 'NONE', #7959, #9611, #5594, .T. ) ;
#8463=ADVANCED_FACE ( 'NONE', ( #7594 ), #7724, .T. ) ;
#8522=DIRECTION ( 'NONE',  ( 0.000000000000000000, 0.000000000000000000, -1.000000000000000000 ) ) ;
#8574=DIRECTION ( 'NONE',  ( 0.9961946980917455452, 1.067350013832296744E-17, 0.08715574274765813811 ) ) ;
#8606=DIRECTION ( 'NONE',  ( -1.000000000000000000, -0.000000000000000000, -0.000000000000000000 ) ) ;
#8627=AXIS2_PLACEMENT_3D ( 'NONE', #12210, #6534, #6349 ) ;
#8628=ORIENTED_EDGE ( 'NONE', *, *, #4658, .F. ) ;
#8741=ORIENTED_EDGE ( 'NONE', *, *, #9926, .F. ) ;
#8765=DIRECTION ( 'NONE',  ( 0.000000000000000000, 0.000000000000000000, 1.000000000000000000 ) ) ;
#8776=DIRECTION ( 'NONE',  ( -0.000000000000000000, 0.000000000000000000, 1.000000000000000000 ) ) ;
#8812=AXIS2_PLACEMENT_3D ( 'NONE', #3831, #2013, #6767 ) ;
#8864=DIRECTION ( 'NONE',  ( 1.000000000000000000, 0.000000000000000000, 0.000000000000000000 ) ) ;
#8889=ORIENTED_EDGE ( 'NONE', *, *, #1294, .T. ) ;
#8909=CARTESIAN_POINT ( 'NONE',  ( 0.000000000000000000, -0.5999999999999996447, -2.622672778259560467 ) ) ;
#8917=EDGE_CURVE ( 'NONE', #972, #9795, #10301, .T. ) ;
#8930=DIRECTION ( 'NONE',  ( 0.000000000000000000, 0.000000000000000000, -1.000000000000000000 ) ) ;
#8932=ORIENTED_EDGE ( 'NONE', *, *, #6661, .F. ) ;
#8940=ORIENTED_EDGE ( 'NONE', *, *, #6661, .T. ) ;
#8950=DIRECTION ( 'NONE',  ( 0.000000000000000000, 0.000000000000000000, 1.000000000000000000 ) ) ;
#8977=TOROIDAL_SURFACE ( 'NONE', #5974, 2.690429798716874377, 1.199999999999999956 ) ;
#9001=AXIS2_PLACEMENT_3D ( 'NONE', #8446, #11487, #3932 ) ;
#9019=AXIS2_PLACEMENT_3D ( 'NONE', #12028, #10221, #7480 ) ;
#9370=( NAMED_UNIT ( * ) SI_UNIT ( $, .STERADIAN. ) SOLID_ANGLE_UNIT ( ) );
#9439=CIRCLE ( 'NONE', #5041, 1.199999999999999956 ) ;
#9491=DIRECTION ( 'NONE',  ( 0.000000000000000000, 0.000000000000000000, 1.000000000000000000 ) ) ;
#9514=CARTESIAN_POINT ( 'NONE',  ( 0.000000000000000000, 4.641444688392526779E-16, 3.790027207537782772 ) ) ;
#9542=UNCERTAINTY_MEASURE_WITH_UNIT (LENGTH_MEASURE( 1.000000000000000082E-05 ), #10397, 'distance_accuracy_value', 'NONE');
#9563=AXIS2_PLACEMENT_3D ( 'NONE', #3879, #4804, #2801 ) ;
#9565=CARTESIAN_POINT ( 'NONE',  ( 0.3697398607305836249, -0.6000000000000000888, 3.517354947232271378 ) ) ;
#9611=VERTEX_POINT ( 'NONE', #11461 ) ;
#9630=CIRCLE ( 'NONE', #7630, 3.885863436426969297 ) ;
#9750=DIRECTION ( 'NONE',  ( -1.000000000000000000, 0.000000000000000000, -0.000000000000000000 ) ) ;
#9762=CARTESIAN_POINT ( 'NONE',  ( 1.095413108702814053, 0.000000000000000000, -3.885863436426969297 ) ) ;
#9777=DIRECTION ( 'NONE',  ( -1.000000000000000000, 0.000000000000000000, -0.000000000000000000 ) ) ;
#9785=B_SPLINE_CURVE_WITH_KNOTS ( 'NONE', 3,
 ( #6754, #5814, #5743, #9565, #1940, #5888, #995, #4810 ),
 .UNSPECIFIED., .F., .F.,
 ( 4, 2, 2, 4 ),
 ( 0.001169467769275536707, 0.002016047890428424548, 0.002439337951004867493, 0.002862628011581310871 ),
 .UNSPECIFIED. ) ;
#9795=VERTEX_POINT ( 'NONE', #10203 ) ;
#9796=MECHANICAL_DESIGN_GEOMETRIC_PRESENTATION_REPRESENTATION('',(#1993),#7194);
#9800=CARTESIAN_POINT ( 'NONE',  ( 0.000000000000000000, 0.5999999999999998668, -2.622672778259560467 ) ) ;
#9871=DIRECTION ( 'NONE',  ( 1.000000000000000000, 0.000000000000000000, 0.000000000000000000 ) ) ;
#9877=DIRECTION ( 'NONE',  ( 1.000000000000000000, 0.000000000000000000, 0.000000000000000000 ) ) ;
#9888=ORIENTED_EDGE ( 'NONE', *, *, #3336, .F. ) ;
#9890=CARTESIAN_POINT ( 'NONE',  ( 1.000000000000000000, 0.5999999999999998668, -4.000000000000000000 ) ) ;
#9904=CONICAL_SURFACE ( 'NONE', #4700, 3.790027207537782772, 0.08726646259971644615 ) ;
#9926=EDGE_CURVE ( 'NONE', #11679, #6664, #5443, .T. ) ;
#9955=CARTESIAN_POINT ( 'NONE',  ( 0.000000000000000000, -0.5999999999999994227, -4.000000000000000000 ) ) ;
#9987=AXIS2_PLACEMENT_3D ( 'NONE', #9890, #1258, #8950 ) ;
#9996=DIRECTION ( 'NONE',  ( 0.000000000000000000, 1.598721155460225103E-14, 1.000000000000000000 ) ) ;
#10017=ORIENTED_EDGE ( 'NONE', *, *, #10534, .T. ) ;
#10018=CARTESIAN_POINT ( 'NONE',  ( 1.000000000000000000, -0.5999999999999995337, -3.826895796574397046 ) ) ;
#10030=( GEOMETRIC_REPRESENTATION_CONTEXT ( 3 ) GLOBAL_UNCERTAINTY_ASSIGNED_CONTEXT ( ( #6666 ) ) GLOBAL_UNIT_ASSIGNED_CONTEXT ( ( #3804, #11241, #9370 ) ) REPRESENTATION_CONTEXT ( 'NONE', 'WORKASPACE' ) );
#10058=CARTESIAN_POINT ( 'NONE',  ( 0.000000000000000000, 0.5999999999999998668, -2.622672778259560467 ) ) ;
#10100=ORIENTED_EDGE ( 'NONE', *, *, #10376, .F. ) ;
#10203=CARTESIAN_POINT ( 'NONE',  ( 0.000000000000000000, 0.5999999999999998668, 2.622672778259560467 ) ) ;
#10221=DIRECTION ( 'NONE',  ( -1.000000000000000000, 0.000000000000000000, -0.000000000000000000 ) ) ;
#10233=AXIS2_PLACEMENT_3D ( 'NONE', #6718, #2017, #10512 ) ;
#10234=AXIS2_PLACEMENT_3D ( 'NONE', #2937, #6755, #2002 ) ;
#10272=VECTOR ( 'NONE', #6725, 1000.000000000000000 ) ;
#10301=B_SPLINE_CURVE_WITH_KNOTS ( 'NONE', 3,
 ( #3372, #4610, #8193, #2865, #549, #496, #10352, #11293, #11419, #5316 ),
 .UNSPECIFIED., .F., .F.,
 ( 4, 2, 2, 2, 4 ),
 ( 0.004762249257309257751, 0.005185715735975977674, 0.005609182214642698464, 0.006032648693309418386, 0.006456115171976138309 ),
 .UNSPECIFIED. ) ;
#10327=ORIENTED_EDGE ( 'NONE', *, *, #560, .T. ) ;
#10341=DIRECTION ( 'NONE',  ( 0.000000000000000000, 0.000000000000000000, 1.000000000000000000 ) ) ;
#10352=CARTESIAN_POINT ( 'NONE',  ( 0.1192621039632846131, 0.5999999999999998668, 3.174418872716579187 ) ) ;
#10376=EDGE_CURVE ( 'NONE', #6297, #5352, #9785, .T. ) ;
#10397=( LENGTH_UNIT ( ) NAMED_UNIT ( * ) SI_UNIT ( .MILLI., .METRE. ) );
#10470=DIRECTION ( 'NONE',  ( 1.000000000000000000, 0.000000000000000000, 0.000000000000000000 ) ) ;
#10477=CARTESIAN_POINT ( 'NONE',  ( -25.39999999999996305, 0.000000000000000000, 0.000000000000000000 ) ) ;
#10512=DIRECTION ( 'NONE',  ( 0.000000000000000000, 0.000000000000000000, 1.000000000000000000 ) ) ;
#10519=UNCERTAINTY_MEASURE_WITH_UNIT (LENGTH_MEASURE( 1.000000000000000082E-05 ), #10862, 'distance_accuracy_value', 'NONE');
#10534=EDGE_CURVE ( 'NONE', #972, #10913, #169, .T. ) ;
#10557=ORIENTED_EDGE ( 'NONE', *, *, #1332, .T. ) ;
#10598=ORIENTED_EDGE ( 'NONE', *, *, #11777, .F. ) ;
#10660=DIRECTION ( 'NONE',  ( 0.000000000000000000, 0.000000000000000000, 1.000000000000000000 ) ) ;
#10699=DIRECTION ( 'NONE',  ( 1.000000000000000000, -0.000000000000000000, -0.000000000000000000 ) ) ;
#10727=CARTESIAN_POINT ( 'NONE',  ( 0.8603238823369437904, 0.5999999999999998668, -3.802997805305113665 ) ) ;
#10745=CARTESIAN_POINT ( 'NONE',  ( -25.39999999999996305, 2.449293598294706414E-16, -2.000000000000000000 ) ) ;
#10779=AXIS2_PLACEMENT_3D ( 'NONE', #8058, #2222, #8115 ) ;
#10835=PLANE ( 'NONE',  #6092 ) ;
#10862=( LENGTH_UNIT ( ) NAMED_UNIT ( * ) SI_UNIT ( .MILLI., .METRE. ) );
#10913=VERTEX_POINT ( 'NONE', #11350 ) ;
#10923=ORIENTED_EDGE ( 'NONE', *, *, #2717, .T. ) ;
#11023=ORIENTED_EDGE ( 'NONE', *, *, #12093, .F. ) ;
#11027=VERTEX_POINT ( 'NONE', #391 ) ;
#11113=DIRECTION ( 'NONE',  ( 1.000000000000000000, 0.000000000000000000, 0.000000000000000000 ) ) ;
#11175=AXIS2_PLACEMENT_3D ( 'NONE', #6700, #9750, #1170 ) ;
#11207=DIRECTION ( 'NONE',  ( 0.000000000000000000, 0.000000000000000000, 1.000000000000000000 ) ) ;
#11224=SHAPE_DEFINITION_REPRESENTATION ( #4619, #5877 ) ;
#11226=PRODUCT_DEFINITION_FORMATION_WITH_SPECIFIED_SOURCE ( 'ANY', '', #7730, .NOT_KNOWN. ) ;
#11241=( NAMED_UNIT ( * ) PLANE_ANGLE_UNIT ( ) SI_UNIT ( $, .RADIAN. ) );
#11286=ORIENTED_EDGE ( 'NONE', *, *, #8917, .F. ) ;
#11293=CARTESIAN_POINT ( 'NONE',  ( 0.02381023875259481032, 0.5999999999999999778, 2.905405940543879240 ) ) ;
#11350=CARTESIAN_POINT ( 'NONE',  ( 1.000000000000000000, 0.000000000000000000, 3.873645755336797780 ) ) ;
#11419=CARTESIAN_POINT ( 'NONE',  ( -1.067261513540418427E-16, 0.5999999999999998668, 2.765611175118570575 ) ) ;
#11461=CARTESIAN_POINT ( 'NONE',  ( 2.399999999999999467, 0.000000000000000000, 2.000000000000000000 ) ) ;
#11487=DIRECTION ( 'NONE',  ( -1.000000000000000000, -0.000000000000000000, -0.000000000000000000 ) ) ;
#11585=AXIS2_PLACEMENT_3D ( 'NONE', #261, #6901, #8765 ) ;
#11607=PLANE ( 'NONE',  #3622 ) ;
#11663=CARTESIAN_POINT ( 'NONE',  ( -3.206358518536427241E-14, 0.5999999999999998668, -2.905281953981669218 ) ) ;
#11671=FACE_OUTER_BOUND ( 'NONE', #6378, .T. ) ;
#11679=VERTEX_POINT ( 'NONE', #4637 ) ;
#11688=CARTESIAN_POINT ( 'NONE',  ( 1.000000000000000000, 0.000000000000000000, 0.000000000000000000 ) ) ;
#11698=EDGE_LOOP ( 'NONE', ( #3944, #2123 ) ) ;
#11699=CARTESIAN_POINT ( 'NONE',  ( 0.000000000000000000, -0.6000000000000000888, 2.622672778259560467 ) ) ;
#11718=SURFACE_STYLE_FILL_AREA ( #11784 ) ;
#11728=DIRECTION ( 'NONE',  ( 1.000000000000000000, -0.000000000000000000, -0.000000000000000000 ) ) ;
#11761=AXIS2_PLACEMENT_3D ( 'NONE', #11688, #10699, #254 ) ;
#11777=EDGE_CURVE ( 'NONE', #5455, #2990, #9439, .T. ) ;
#11778=EDGE_LOOP ( 'NONE', ( #8889, #8173, #10327, #9888 ) ) ;
#11784=FILL_AREA_STYLE ('',( #5931 ) ) ;
#11888=ORIENTED_EDGE ( 'NONE', *, *, #3810, .F. ) ;
#11893=EDGE_CURVE ( 'NONE', #11679, #7959, #2358, .T. ) ;
#11983=AXIS2_PLACEMENT_3D ( 'NONE', #2978, #5675, #6802 ) ;
#11999=ORIENTED_EDGE ( 'NONE', *, *, #3023, .F. ) ;
#12028=CARTESIAN_POINT ( 'NONE',  ( -7.839872433920653082E-18, 0.000000000000000000, 0.000000000000000000 ) ) ;
#12039=VERTEX_POINT ( 'NONE', #8063 ) ;
#12061=ORIENTED_EDGE ( 'NONE', *, *, #1273, .F. ) ;
#12068=VECTOR ( 'NONE', #8574, 1000.000000000000000 ) ;
#12093=EDGE_CURVE ( 'NONE', #9795, #6083, #405, .T. ) ;
#12113=CARTESIAN_POINT ( 'NONE',  ( 0.000000000000000000, -0.5999999999999996447, -2.622672778259560467 ) ) ;
#12125=EDGE_LOOP ( 'NONE', ( #5867, #8932, #158, #4450, #8628, #11888 ) ) ;
#12207=PLANE ( 'NONE',  #9019 ) ;
#12210=CARTESIAN_POINT ( 'NONE',  ( 0.000000000000000000, 0.000000000000000000, 0.000000000000000000 ) ) ;
#12275=ORIENTED_EDGE ( 'NONE', *, *, #9926, .T. ) ;
#12282=DIRECTION ( 'NONE',  ( -1.000000000000000000, -0.000000000000000000, -0.000000000000000000 ) ) ;
#12283=DIRECTION ( 'NONE',  ( 0.000000000000000000, 0.000000000000000000, 1.000000000000000000 ) ) ;
#12399=COLOUR_RGB('Black',0.12,0.14,0.17);
#12400=FILL_AREA_STYLE_COLOUR('',#12399);
#12401=FILL_AREA_STYLE('',(#12400));
#12402=SURFACE_STYLE_FILL_AREA(#12401);
#12403=SURFACE_SIDE_STYLE('',(#12402));
#12404=SURFACE_STYLE_USAGE(.BOTH.,#12403);
#12405=PRESENTATION_STYLE_ASSIGNMENT((#12404));
ENDSEC;
END-ISO-10303-21;
